ISO-10303-21;
HEADER;
/* Generated by software containing ST-Developer
 * from STEP Tools, Inc. (www.steptools.com) 
 */

FILE_DESCRIPTION(
/* description */ ('PAT-091'),
/* implementation_level */ '2;1');

FILE_NAME(
/* name */ 'M4x10 Cap Screw.step',
/* time_stamp */ '2026-10-27T15:34:44-07:00',
/* author */ (''),
/* organization */ (''),
/* preprocessor_version */ 'ST-DEVELOPER v20.2',
/* originating_system */ 'Autodesk Translation Framework v15.17.0.0',
/* authorisation */ '');

FILE_SCHEMA (('AUTOMOTIVE_DESIGN { 1 0 10303 214 3 1 1 }'));
ENDSEC;

DATA;
#10=MECHANICAL_DESIGN_GEOMETRIC_PRESENTATION_REPRESENTATION('',(#988),#25100);
#729=CONICAL_SURFACE('',#14907,0.325,0.785398163397448);
#730=CONICAL_SURFACE('',#14911,0.335,0.785398163397448);
#731=CONICAL_SURFACE('',#14915,0.21,0.463647609000806);
#745=ORIENTED_CLOSED_SHELL('',*,#13265,.F.);
#748=BREP_WITH_VOIDS('Body1',#13266,(#745));
#768=SHAPE_REPRESENTATION_RELATIONSHIP('SRR','None',#25529,#878);
#878=ADVANCED_BREP_SHAPE_REPRESENTATION('',(#748),#24999);
#988=STYLED_ITEM('',(#26198),#748);
#1333=FACE_BOUND('',#3155,.T.);
#1708=PLANE('',#14895);
#1709=PLANE('',#14896);
#1710=PLANE('',#14897);
#1711=PLANE('',#14898);
#1712=PLANE('',#14899);
#1713=PLANE('',#14900);
#1714=PLANE('',#14901);
#1715=PLANE('',#14902);
#1716=PLANE('',#14903);
#1717=PLANE('',#14905);
#1718=PLANE('',#14913);
#2205=FACE_OUTER_BOUND('',#3141,.T.);
#2206=FACE_OUTER_BOUND('',#3142,.T.);
#2207=FACE_OUTER_BOUND('',#3143,.T.);
#2208=FACE_OUTER_BOUND('',#3144,.T.);
#2209=FACE_OUTER_BOUND('',#3145,.T.);
#2210=FACE_OUTER_BOUND('',#3146,.T.);
#2211=FACE_OUTER_BOUND('',#3147,.T.);
#2212=FACE_OUTER_BOUND('',#3148,.T.);
#2213=FACE_OUTER_BOUND('',#3149,.T.);
#2214=FACE_OUTER_BOUND('',#3150,.T.);
#2215=FACE_OUTER_BOUND('',#3151,.T.);
#2216=FACE_OUTER_BOUND('',#3152,.T.);
#2217=FACE_OUTER_BOUND('',#3153,.T.);
#2218=FACE_OUTER_BOUND('',#3154,.T.);
#2219=FACE_OUTER_BOUND('',#3156,.T.);
#2220=FACE_OUTER_BOUND('',#3157,.T.);
#3141=EDGE_LOOP('',(#9584,#9585,#9586,#9587));
#3142=EDGE_LOOP('',(#9588,#9589,#9590,#9591));
#3143=EDGE_LOOP('',(#9592,#9593,#9594,#9595));
#3144=EDGE_LOOP('',(#9596,#9597,#9598,#9599));
#3145=EDGE_LOOP('',(#9600,#9601,#9602,#9603));
#3146=EDGE_LOOP('',(#9604,#9605,#9606,#9607));
#3147=EDGE_LOOP('',(#9608,#9609,#9610,#9611,#9612,#9613));
#3148=EDGE_LOOP('',(#9614,#9615,#9616,#9617,#9618,#9619));
#3149=EDGE_LOOP('',(#9620));
#3150=EDGE_LOOP('',(#9621));
#3151=EDGE_LOOP('',(#9622,#9623,#9624,#9625));
#3152=EDGE_LOOP('',(#9626,#9627,#9628,#9629));
#3153=EDGE_LOOP('',(#9630,#9631,#9632,#9633));
#3154=EDGE_LOOP('',(#9634));
#3155=EDGE_LOOP('',(#9635));
#3156=EDGE_LOOP('',(#9636,#9637,#9638,#9639));
#3157=EDGE_LOOP('',(#9640,#9641,#9642,#9643));
#4282=LINE('',#21649,#5022);
#4283=LINE('',#21651,#5023);
#4284=LINE('',#21653,#5024);
#4285=LINE('',#21654,#5025);
#4286=LINE('',#21657,#5026);
#4287=LINE('',#21659,#5027);
#4288=LINE('',#21660,#5028);
#4289=LINE('',#21663,#5029);
#4290=LINE('',#21665,#5030);
#4291=LINE('',#21666,#5031);
#4292=LINE('',#21669,#5032);
#4293=LINE('',#21671,#5033);
#4294=LINE('',#21672,#5034);
#4295=LINE('',#21675,#5035);
#4296=LINE('',#21677,#5036);
#4297=LINE('',#21678,#5037);
#4298=LINE('',#21680,#5038);
#4299=LINE('',#21681,#5039);
#4300=LINE('',#21693,#5040);
#4301=LINE('',#21697,#5041);
#4302=LINE('',#21701,#5042);
#4303=LINE('',#21708,#5043);
#4304=LINE('',#21710,#5044);
#5022=VECTOR('',#17248,1.);
#5023=VECTOR('',#17249,1.);
#5024=VECTOR('',#17250,1.);
#5025=VECTOR('',#17251,1.);
#5026=VECTOR('',#17254,1.);
#5027=VECTOR('',#17255,1.);
#5028=VECTOR('',#17256,1.);
#5029=VECTOR('',#17259,1.);
#5030=VECTOR('',#17260,1.);
#5031=VECTOR('',#17261,1.);
#5032=VECTOR('',#17264,1.);
#5033=VECTOR('',#17265,1.);
#5034=VECTOR('',#17266,1.);
#5035=VECTOR('',#17269,1.);
#5036=VECTOR('',#17270,1.);
#5037=VECTOR('',#17271,1.);
#5038=VECTOR('',#17274,1.);
#5039=VECTOR('',#17275,1.);
#5040=VECTOR('',#17292,0.325);
#5041=VECTOR('',#17297,0.35);
#5042=VECTOR('',#17302,0.335);
#5043=VECTOR('',#17311,0.21);
#5044=VECTOR('',#17314,0.2);
#5752=CIRCLE('',#14904,0.1954);
#5753=CIRCLE('',#14906,0.3);
#5754=CIRCLE('',#14908,0.35);
#5755=CIRCLE('',#14910,0.35);
#5756=CIRCLE('',#14912,0.32);
#5757=CIRCLE('',#14914,0.22);
#5758=CIRCLE('',#14916,0.1954);
#6587=VERTEX_POINT('',#21647);
#6588=VERTEX_POINT('',#21648);
#6589=VERTEX_POINT('',#21650);
#6590=VERTEX_POINT('',#21652);
#6591=VERTEX_POINT('',#21656);
#6592=VERTEX_POINT('',#21658);
#6593=VERTEX_POINT('',#21662);
#6594=VERTEX_POINT('',#21664);
#6595=VERTEX_POINT('',#21668);
#6596=VERTEX_POINT('',#21670);
#6597=VERTEX_POINT('',#21674);
#6598=VERTEX_POINT('',#21676);
#6599=VERTEX_POINT('',#21685);
#6600=VERTEX_POINT('',#21688);
#6601=VERTEX_POINT('',#21691);
#6602=VERTEX_POINT('',#21695);
#6603=VERTEX_POINT('',#21699);
#6604=VERTEX_POINT('',#21703);
#6605=VERTEX_POINT('',#21706);
#7727=EDGE_CURVE('',#6587,#6588,#4282,.T.);
#7728=EDGE_CURVE('',#6588,#6589,#4283,.T.);
#7729=EDGE_CURVE('',#6589,#6590,#4284,.T.);
#7730=EDGE_CURVE('',#6587,#6590,#4285,.T.);
#7731=EDGE_CURVE('',#6588,#6591,#4286,.T.);
#7732=EDGE_CURVE('',#6591,#6592,#4287,.T.);
#7733=EDGE_CURVE('',#6592,#6589,#4288,.T.);
#7734=EDGE_CURVE('',#6591,#6593,#4289,.T.);
#7735=EDGE_CURVE('',#6593,#6594,#4290,.T.);
#7736=EDGE_CURVE('',#6594,#6592,#4291,.T.);
#7737=EDGE_CURVE('',#6593,#6595,#4292,.T.);
#7738=EDGE_CURVE('',#6595,#6596,#4293,.T.);
#7739=EDGE_CURVE('',#6596,#6594,#4294,.T.);
#7740=EDGE_CURVE('',#6595,#6597,#4295,.T.);
#7741=EDGE_CURVE('',#6597,#6598,#4296,.T.);
#7742=EDGE_CURVE('',#6598,#6596,#4297,.T.);
#7743=EDGE_CURVE('',#6597,#6587,#4298,.T.);
#7744=EDGE_CURVE('',#6590,#6598,#4299,.T.);
#7745=EDGE_CURVE('',#6599,#6599,#5752,.T.);
#7746=EDGE_CURVE('',#6600,#6600,#5753,.T.);
#7747=EDGE_CURVE('',#6601,#6601,#5754,.T.);
#7748=EDGE_CURVE('',#6601,#6600,#4300,.T.);
#7749=EDGE_CURVE('',#6602,#6602,#5755,.T.);
#7750=EDGE_CURVE('',#6602,#6601,#4301,.T.);
#7751=EDGE_CURVE('',#6603,#6603,#5756,.T.);
#7752=EDGE_CURVE('',#6603,#6602,#4302,.T.);
#7753=EDGE_CURVE('',#6604,#6604,#5757,.T.);
#7754=EDGE_CURVE('',#6605,#6605,#5758,.F.);
#7755=EDGE_CURVE('',#6605,#6604,#4303,.T.);
#7756=EDGE_CURVE('',#6599,#6605,#4304,.T.);
#9584=ORIENTED_EDGE('',*,*,#7727,.T.);
#9585=ORIENTED_EDGE('',*,*,#7728,.T.);
#9586=ORIENTED_EDGE('',*,*,#7729,.T.);
#9587=ORIENTED_EDGE('',*,*,#7730,.F.);
#9588=ORIENTED_EDGE('',*,*,#7731,.T.);
#9589=ORIENTED_EDGE('',*,*,#7732,.T.);
#9590=ORIENTED_EDGE('',*,*,#7733,.T.);
#9591=ORIENTED_EDGE('',*,*,#7728,.F.);
#9592=ORIENTED_EDGE('',*,*,#7734,.T.);
#9593=ORIENTED_EDGE('',*,*,#7735,.T.);
#9594=ORIENTED_EDGE('',*,*,#7736,.T.);
#9595=ORIENTED_EDGE('',*,*,#7732,.F.);
#9596=ORIENTED_EDGE('',*,*,#7737,.T.);
#9597=ORIENTED_EDGE('',*,*,#7738,.T.);
#9598=ORIENTED_EDGE('',*,*,#7739,.T.);
#9599=ORIENTED_EDGE('',*,*,#7735,.F.);
#9600=ORIENTED_EDGE('',*,*,#7740,.T.);
#9601=ORIENTED_EDGE('',*,*,#7741,.T.);
#9602=ORIENTED_EDGE('',*,*,#7742,.T.);
#9603=ORIENTED_EDGE('',*,*,#7738,.F.);
#9604=ORIENTED_EDGE('',*,*,#7743,.T.);
#9605=ORIENTED_EDGE('',*,*,#7730,.T.);
#9606=ORIENTED_EDGE('',*,*,#7744,.T.);
#9607=ORIENTED_EDGE('',*,*,#7741,.F.);
#9608=ORIENTED_EDGE('',*,*,#7743,.F.);
#9609=ORIENTED_EDGE('',*,*,#7740,.F.);
#9610=ORIENTED_EDGE('',*,*,#7737,.F.);
#9611=ORIENTED_EDGE('',*,*,#7734,.F.);
#9612=ORIENTED_EDGE('',*,*,#7731,.F.);
#9613=ORIENTED_EDGE('',*,*,#7727,.F.);
#9614=ORIENTED_EDGE('',*,*,#7744,.F.);
#9615=ORIENTED_EDGE('',*,*,#7729,.F.);
#9616=ORIENTED_EDGE('',*,*,#7733,.F.);
#9617=ORIENTED_EDGE('',*,*,#7736,.F.);
#9618=ORIENTED_EDGE('',*,*,#7739,.F.);
#9619=ORIENTED_EDGE('',*,*,#7742,.F.);
#9620=ORIENTED_EDGE('',*,*,#7745,.F.);
#9621=ORIENTED_EDGE('',*,*,#7746,.F.);
#9622=ORIENTED_EDGE('',*,*,#7747,.F.);
#9623=ORIENTED_EDGE('',*,*,#7748,.T.);
#9624=ORIENTED_EDGE('',*,*,#7746,.T.);
#9625=ORIENTED_EDGE('',*,*,#7748,.F.);
#9626=ORIENTED_EDGE('',*,*,#7749,.F.);
#9627=ORIENTED_EDGE('',*,*,#7750,.T.);
#9628=ORIENTED_EDGE('',*,*,#7747,.T.);
#9629=ORIENTED_EDGE('',*,*,#7750,.F.);
#9630=ORIENTED_EDGE('',*,*,#7751,.F.);
#9631=ORIENTED_EDGE('',*,*,#7752,.T.);
#9632=ORIENTED_EDGE('',*,*,#7749,.T.);
#9633=ORIENTED_EDGE('',*,*,#7752,.F.);
#9634=ORIENTED_EDGE('',*,*,#7751,.T.);
#9635=ORIENTED_EDGE('',*,*,#7753,.F.);
#9636=ORIENTED_EDGE('',*,*,#7754,.F.);
#9637=ORIENTED_EDGE('',*,*,#7755,.T.);
#9638=ORIENTED_EDGE('',*,*,#7753,.T.);
#9639=ORIENTED_EDGE('',*,*,#7755,.F.);
#9640=ORIENTED_EDGE('',*,*,#7745,.T.);
#9641=ORIENTED_EDGE('',*,*,#7756,.T.);
#9642=ORIENTED_EDGE('',*,*,#7754,.T.);
#9643=ORIENTED_EDGE('',*,*,#7756,.F.);
#12148=CYLINDRICAL_SURFACE('',#14909,0.35);
#12149=CYLINDRICAL_SURFACE('',#14917,0.1954);
#12572=ADVANCED_FACE('',(#2205),#1708,.F.);
#12573=ADVANCED_FACE('',(#2206),#1709,.F.);
#12574=ADVANCED_FACE('',(#2207),#1710,.F.);
#12575=ADVANCED_FACE('',(#2208),#1711,.F.);
#12576=ADVANCED_FACE('',(#2209),#1712,.F.);
#12577=ADVANCED_FACE('',(#2210),#1713,.F.);
#12578=ADVANCED_FACE('',(#2211),#1714,.F.);
#12579=ADVANCED_FACE('',(#2212),#1715,.F.);
#12580=ADVANCED_FACE('',(#2213),#1716,.F.);
#12581=ADVANCED_FACE('',(#2214),#1717,.T.);
#12582=ADVANCED_FACE('',(#2215),#729,.T.);
#12583=ADVANCED_FACE('',(#2216),#12148,.T.);
#12584=ADVANCED_FACE('',(#2217),#730,.T.);
#12585=ADVANCED_FACE('',(#2218,#1333),#1718,.T.);
#12586=ADVANCED_FACE('',(#2219),#731,.T.);
#12587=ADVANCED_FACE('',(#2220),#12149,.T.);
#13265=CLOSED_SHELL('',(#12572,#12573,#12574,#12575,#12576,#12577,#12578,
#12579));
#13266=CLOSED_SHELL('',(#12580,#12581,#12582,#12583,#12584,#12585,#12586,
#12587));
#14894=AXIS2_PLACEMENT_3D('',#21645,#17244,#17245);
#14895=AXIS2_PLACEMENT_3D('',#21646,#17246,#17247);
#14896=AXIS2_PLACEMENT_3D('',#21655,#17252,#17253);
#14897=AXIS2_PLACEMENT_3D('',#21661,#17257,#17258);
#14898=AXIS2_PLACEMENT_3D('',#21667,#17262,#17263);
#14899=AXIS2_PLACEMENT_3D('',#21673,#17267,#17268);
#14900=AXIS2_PLACEMENT_3D('',#21679,#17272,#17273);
#14901=AXIS2_PLACEMENT_3D('',#21682,#17276,#17277);
#14902=AXIS2_PLACEMENT_3D('',#21683,#17278,#17279);
#14903=AXIS2_PLACEMENT_3D('',#21684,#17280,#17281);
#14904=AXIS2_PLACEMENT_3D('',#21686,#17282,#17283);
#14905=AXIS2_PLACEMENT_3D('',#21687,#17284,#17285);
#14906=AXIS2_PLACEMENT_3D('',#21689,#17286,#17287);
#14907=AXIS2_PLACEMENT_3D('',#21690,#17288,#17289);
#14908=AXIS2_PLACEMENT_3D('',#21692,#17290,#17291);
#14909=AXIS2_PLACEMENT_3D('',#21694,#17293,#17294);
#14910=AXIS2_PLACEMENT_3D('',#21696,#17295,#17296);
#14911=AXIS2_PLACEMENT_3D('',#21698,#17298,#17299);
#14912=AXIS2_PLACEMENT_3D('',#21700,#17300,#17301);
#14913=AXIS2_PLACEMENT_3D('',#21702,#17303,#17304);
#14914=AXIS2_PLACEMENT_3D('',#21704,#17305,#17306);
#14915=AXIS2_PLACEMENT_3D('',#21705,#17307,#17308);
#14916=AXIS2_PLACEMENT_3D('',#21707,#17309,#17310);
#14917=AXIS2_PLACEMENT_3D('',#21709,#17312,#17313);
#17244=DIRECTION('axis',(0.,0.,1.));
#17245=DIRECTION('refdir',(1.,0.,0.));
#17246=DIRECTION('center_axis',(0.866025403784439,0.,-0.5));
#17247=DIRECTION('ref_axis',(0.5,0.,0.866025403784439));
#17248=DIRECTION('',(-0.5,0.,-0.866025403784439));
#17249=DIRECTION('',(0.,-1.,0.));
#17250=DIRECTION('',(0.5,0.,0.866025403784439));
#17251=DIRECTION('',(0.,-1.,0.));
#17252=DIRECTION('center_axis',(1.60246890531964E-16,0.,-1.));
#17253=DIRECTION('ref_axis',(1.,0.,1.60246890531964E-16));
#17254=DIRECTION('',(-1.,0.,-1.60246890531964E-16));
#17255=DIRECTION('',(0.,-1.,0.));
#17256=DIRECTION('',(1.,0.,1.60246890531964E-16));
#17257=DIRECTION('center_axis',(-0.866025403784439,0.,-0.5));
#17258=DIRECTION('ref_axis',(0.5,0.,-0.866025403784439));
#17259=DIRECTION('',(-0.5,0.,0.866025403784439));
#17260=DIRECTION('',(0.,-1.,0.));
#17261=DIRECTION('',(0.5,0.,-0.866025403784439));
#17262=DIRECTION('center_axis',(-0.866025403784439,0.,0.5));
#17263=DIRECTION('ref_axis',(-0.5,0.,-0.866025403784439));
#17264=DIRECTION('',(0.5,0.,0.866025403784439));
#17265=DIRECTION('',(0.,-1.,0.));
#17266=DIRECTION('',(-0.5,0.,-0.866025403784439));
#17267=DIRECTION('center_axis',(-1.60246890531964E-16,0.,1.));
#17268=DIRECTION('ref_axis',(-1.,0.,-1.60246890531964E-16));
#17269=DIRECTION('',(1.,0.,1.60246890531964E-16));
#17270=DIRECTION('',(0.,-1.,0.));
#17271=DIRECTION('',(-1.,0.,-1.60246890531964E-16));
#17272=DIRECTION('center_axis',(0.866025403784439,0.,0.5));
#17273=DIRECTION('ref_axis',(-0.5,0.,0.866025403784439));
#17274=DIRECTION('',(0.5,0.,-0.866025403784439));
#17275=DIRECTION('',(-0.5,0.,0.866025403784439));
#17276=DIRECTION('center_axis',(0.,1.,0.));
#17277=DIRECTION('ref_axis',(1.,0.,0.));
#17278=DIRECTION('center_axis',(0.,-1.,0.));
#17279=DIRECTION('ref_axis',(0.,0.,-1.));
#17280=DIRECTION('center_axis',(0.,1.,0.));
#17281=DIRECTION('ref_axis',(1.,0.,0.));
#17282=DIRECTION('center_axis',(0.,1.,0.));
#17283=DIRECTION('ref_axis',(1.,0.,0.));
#17284=DIRECTION('center_axis',(0.,1.,0.));
#17285=DIRECTION('ref_axis',(0.,0.,1.));
#17286=DIRECTION('center_axis',(0.,-1.,0.));
#17287=DIRECTION('ref_axis',(1.,0.,0.));
#17288=DIRECTION('center_axis',(0.,-1.,0.));
#17289=DIRECTION('ref_axis',(1.,0.,0.));
#17290=DIRECTION('center_axis',(0.,-1.,0.));
#17291=DIRECTION('ref_axis',(1.,0.,0.));
#17292=DIRECTION('',(0.707106781186547,0.707106781186548,8.65956056235493E-17));
#17293=DIRECTION('center_axis',(0.,-1.,0.));
#17294=DIRECTION('ref_axis',(1.,0.,0.));
#17295=DIRECTION('center_axis',(0.,-1.,0.));
#17296=DIRECTION('ref_axis',(1.,0.,0.));
#17297=DIRECTION('',(0.,1.,0.));
#17298=DIRECTION('center_axis',(0.,1.,0.));
#17299=DIRECTION('ref_axis',(1.,0.,0.));
#17300=DIRECTION('center_axis',(0.,-1.,0.));
#17301=DIRECTION('ref_axis',(1.,0.,0.));
#17302=DIRECTION('',(-0.707106781186547,0.707106781186548,-8.65956056235493E-17));
#17303=DIRECTION('center_axis',(0.,-1.,0.));
#17304=DIRECTION('ref_axis',(0.,0.,-1.));
#17305=DIRECTION('center_axis',(0.,-1.,0.));
#17306=DIRECTION('ref_axis',(1.,0.,0.));
#17307=DIRECTION('center_axis',(0.,1.,0.));
#17308=DIRECTION('ref_axis',(1.,0.,0.));
#17309=DIRECTION('center_axis',(0.,1.,0.));
#17310=DIRECTION('ref_axis',(1.,0.,0.));
#17311=DIRECTION('',(-0.447213595499958,0.894427190999916,-5.47678698264203E-17));
#17312=DIRECTION('center_axis',(0.,-1.,0.));
#17313=DIRECTION('ref_axis',(1.,0.,0.));
#17314=DIRECTION('',(0.,1.,0.));
#21645=CARTESIAN_POINT('',(0.,0.,0.));
#21646=CARTESIAN_POINT('Origin',(0.0866025403784439,-0.4,-0.15));
#21647=CARTESIAN_POINT('',(0.173205080756888,-0.4,0.));
#21648=CARTESIAN_POINT('',(0.0866025403784439,-0.4,-0.15));
#21649=CARTESIAN_POINT('',(0.173205080756888,-0.4,0.));
#21650=CARTESIAN_POINT('',(0.0866025403784439,-0.64,-0.15));
#21651=CARTESIAN_POINT('',(0.0866025403784439,-0.4,-0.15));
#21652=CARTESIAN_POINT('',(0.173205080756888,-0.64,0.));
#21653=CARTESIAN_POINT('',(0.173205080756888,-0.64,0.));
#21654=CARTESIAN_POINT('',(0.173205080756888,-0.4,0.));
#21655=CARTESIAN_POINT('Origin',(-0.0866025403784438,-0.4,-0.15));
#21656=CARTESIAN_POINT('',(-0.0866025403784438,-0.4,-0.15));
#21657=CARTESIAN_POINT('',(0.0866025403784439,-0.4,-0.15));
#21658=CARTESIAN_POINT('',(-0.0866025403784438,-0.64,-0.15));
#21659=CARTESIAN_POINT('',(-0.0866025403784438,-0.4,-0.15));
#21660=CARTESIAN_POINT('',(0.0866025403784439,-0.64,-0.15));
#21661=CARTESIAN_POINT('Origin',(-0.173205080756888,-0.4,-2.77555756156289E-17));
#21662=CARTESIAN_POINT('',(-0.173205080756888,-0.4,-2.12115047744981E-17));
#21663=CARTESIAN_POINT('',(-0.0866025403784438,-0.4,-0.15));
#21664=CARTESIAN_POINT('',(-0.173205080756888,-0.64,-2.77555756156289E-17));
#21665=CARTESIAN_POINT('',(-0.173205080756888,-0.4,-2.12115047744981E-17));
#21666=CARTESIAN_POINT('',(-0.0866025403784438,-0.64,-0.15));
#21667=CARTESIAN_POINT('Origin',(-0.0866025403784439,-0.4,0.15));
#21668=CARTESIAN_POINT('',(-0.0866025403784439,-0.4,0.15));
#21669=CARTESIAN_POINT('',(-0.173205080756888,-0.4,-2.12115047744981E-17));
#21670=CARTESIAN_POINT('',(-0.0866025403784439,-0.64,0.15));
#21671=CARTESIAN_POINT('',(-0.0866025403784439,-0.4,0.15));
#21672=CARTESIAN_POINT('',(-0.173205080756888,-0.64,-2.12115047744981E-17));
#21673=CARTESIAN_POINT('Origin',(0.0866025403784439,-0.4,0.15));
#21674=CARTESIAN_POINT('',(0.0866025403784439,-0.4,0.15));
#21675=CARTESIAN_POINT('',(-0.0866025403784439,-0.4,0.15));
#21676=CARTESIAN_POINT('',(0.0866025403784439,-0.64,0.15));
#21677=CARTESIAN_POINT('',(0.0866025403784439,-0.4,0.15));
#21678=CARTESIAN_POINT('',(-0.0866025403784439,-0.64,0.15));
#21679=CARTESIAN_POINT('Origin',(0.173205080756888,-0.4,0.));
#21680=CARTESIAN_POINT('',(0.0866025403784439,-0.4,0.15));
#21681=CARTESIAN_POINT('',(0.0866025403784439,-0.64,0.15));
#21682=CARTESIAN_POINT('Origin',(0.,-0.4,-2.77555756156289E-17));
#21683=CARTESIAN_POINT('Origin',(0.,-0.64,-2.77555756156289E-17));
#21684=CARTESIAN_POINT('Origin',(0.,-1.,0.));
#21685=CARTESIAN_POINT('',(-0.1954,-1.,2.39295984553393E-17));
#21686=CARTESIAN_POINT('Origin',(0.,-1.,0.));
#21687=CARTESIAN_POINT('Origin',(0.3,0.4,0.));
#21688=CARTESIAN_POINT('',(-0.3,0.4,-3.67394039744206E-17));
#21689=CARTESIAN_POINT('Origin',(0.,0.4,0.));
#21690=CARTESIAN_POINT('Origin',(0.,0.375,0.));
#21691=CARTESIAN_POINT('',(-0.35,0.35,-4.28626379701573E-17));
#21692=CARTESIAN_POINT('Origin',(0.,0.35,0.));
#21693=CARTESIAN_POINT('',(-0.325,0.375,-3.9801020972289E-17));
#21694=CARTESIAN_POINT('Origin',(0.,0.19,0.));
#21695=CARTESIAN_POINT('',(-0.35,0.03,-4.28626379701574E-17));
#21696=CARTESIAN_POINT('Origin',(0.,0.03,0.));
#21697=CARTESIAN_POINT('',(-0.35,0.19,-4.28626379701574E-17));
#21698=CARTESIAN_POINT('Origin',(0.,0.0149999999999999,0.));
#21699=CARTESIAN_POINT('',(-0.32,-3.29597460435593E-17,-3.91886975727153E-17));
#21700=CARTESIAN_POINT('Origin',(0.,0.,0.));
#21701=CARTESIAN_POINT('',(-0.335,0.0149999999999999,-4.10256677714363E-17));
#21702=CARTESIAN_POINT('Origin',(0.22,0.,0.));
#21703=CARTESIAN_POINT('',(-0.22,-6.93889390390723E-18,-2.69422295812418E-17));
#21704=CARTESIAN_POINT('Origin',(0.,0.,0.));
#21705=CARTESIAN_POINT('Origin',(0.,-0.02,0.));
#21706=CARTESIAN_POINT('',(-0.1954,-0.0492,2.39295984553393E-17));
#21707=CARTESIAN_POINT('Origin',(0.,-0.0492,0.));
#21708=CARTESIAN_POINT('',(-0.21,-0.02,-2.57175827820944E-17));
#21709=CARTESIAN_POINT('Origin',(0.,-0.8,0.));
#21710=CARTESIAN_POINT('',(-0.1954,-0.8,-2.39295984553393E-17));
#24878=UNCERTAINTY_MEASURE_WITH_UNIT(LENGTH_MEASURE(0.001),#25101,
'DISTANCE_ACCURACY_VALUE',
'Maximum model space distance between geometric entities at asserted c
onnectivities');
#24979=UNCERTAINTY_MEASURE_WITH_UNIT(LENGTH_MEASURE(0.001),#25101,
'DISTANCE_ACCURACY_VALUE',
'Maximum model space distance between geometric entities at asserted c
onnectivities');
#24999=(
GEOMETRIC_REPRESENTATION_CONTEXT(3)
GLOBAL_UNCERTAINTY_ASSIGNED_CONTEXT((#24878))
GLOBAL_UNIT_ASSIGNED_CONTEXT((#25101,#25103,#25104))
REPRESENTATION_CONTEXT('','3D')
);
#25100=(
GEOMETRIC_REPRESENTATION_CONTEXT(3)
GLOBAL_UNCERTAINTY_ASSIGNED_CONTEXT((#24979))
GLOBAL_UNIT_ASSIGNED_CONTEXT((#25101,#25103,#25104))
REPRESENTATION_CONTEXT('','3D')
);
#25101=(
LENGTH_UNIT()
NAMED_UNIT(*)
SI_UNIT(.CENTI.,.METRE.)
);
#25103=(
NAMED_UNIT(*)
PLANE_ANGLE_UNIT()
SI_UNIT($,.RADIAN.)
);
#25104=(
NAMED_UNIT(*)
SI_UNIT($,.STERADIAN.)
SOLID_ANGLE_UNIT()
);
#25124=SHAPE_DEFINITION_REPRESENTATION(#25244,#25529);
#25244=PRODUCT_DEFINITION_SHAPE('',$,#25650);
#25529=SHAPE_REPRESENTATION('',(#14894),#24999);
#25630=PRODUCT_DEFINITION_CONTEXT('part definition',#25992,'design');
#25650=PRODUCT_DEFINITION('M4x10 Cap Screw','M4x10 Cap Screw',#25770,#25630);
#25770=PRODUCT_DEFINITION_FORMATION('',$,#26013);
#25992=APPLICATION_CONTEXT(
'Core Data for Automotive Mechanical Design Process');
#25993=PRODUCT_CONTEXT('part definition',#25992,'mechanical');
#26013=PRODUCT('M4x10 Cap Screw','M4x10 Cap Screw','M4x10 Cap Screw',(#25993));
#26192=COLOUR_RGB('Black',0.12,0.14,0.17);
#26193=FILL_AREA_STYLE_COLOUR('',#26192);
#26194=FILL_AREA_STYLE('',(#26193));
#26195=SURFACE_STYLE_FILL_AREA(#26194);
#26196=SURFACE_SIDE_STYLE('',(#26195));
#26197=SURFACE_STYLE_USAGE(.BOTH.,#26196);
#26198=PRESENTATION_STYLE_ASSIGNMENT((#26197));
ENDSEC;
END-ISO-10303-21;
